ISO-10303-21;
HEADER;
FILE_DESCRIPTION (('STEP AP214'),
    '1' );
FILE_NAME ('angular contact ball bearing_68_iso_ISO 15 ABB - 1710 - 20,SI,NC,20_68.step',
    '2026-10-04T07:23:31',
    ( '' ),
    ( '' ),
    'SwSTEP 2.0',
    'SolidWorks 2026',
    '' );
FILE_SCHEMA (( 'AUTOMOTIVE_DESIGN' ));
ENDSEC;

DATA;
#27=CARTESIAN_POINT ( 'NONE',  ( -1.399999999999998579, 1.126651916477733026E-15, 7.500000000000007994 ) ) ;
#42=AXIS2_PLACEMENT_3D ( 'NONE', #2337, #7419, #8866 ) ;
#82=ORIENTED_EDGE ( 'NONE', *, *, #3385, .T. ) ;
#87=FACE_OUTER_BOUND ( 'NONE', #4011, .T. ) ;
#94=EDGE_CURVE ( 'NONE', #2407, #2818, #6149, .T. ) ;
#105=ADVANCED_FACE ( 'NONE', ( #143 ), #1537, .T. ) ;
#108=DIRECTION ( 'NONE',  ( 0.000000000000000000, -2.775557561562888270E-17, -1.000000000000000000 ) ) ;
#109=CARTESIAN_POINT ( 'NONE',  ( -20.63749999999999929, 0.000000000000000000, 0.000000000000000000 ) ) ;
#123=ORIENTED_EDGE ( 'NONE', *, *, #7539, .F. ) ;
#143=FACE_OUTER_BOUND ( 'NONE', #4066, .T. ) ;
#148=DIRECTION ( 'NONE',  ( 1.000000000000000000, 0.000000000000000000, 0.000000000000000000 ) ) ;
#167=DIRECTION ( 'NONE',  ( 0.000000000000000000, 2.775557561562888270E-17, 1.000000000000000000 ) ) ;
#180=CIRCLE ( 'NONE', #5817, 7.500000000000007994 ) ;
#207=CYLINDRICAL_SURFACE ( 'NONE', #8878, 5.750000000000006217 ) ;
#232=PLANE ( 'NONE',  #3563 ) ;
#271=ORIENTED_EDGE ( 'NONE', *, *, #10865, .F. ) ;
#310=( GEOMETRIC_REPRESENTATION_CONTEXT ( 3 ) GLOBAL_UNCERTAINTY_ASSIGNED_CONTEXT ( ( #8038 ) ) GLOBAL_UNIT_ASSIGNED_CONTEXT ( ( #3651, #958, #5094 ) ) REPRESENTATION_CONTEXT ( 'NONE', 'WORKASPACE' ) );
#373=AXIS2_PLACEMENT_3D ( 'NONE', #6188, #3894, #6488 ) ;
#409=CIRCLE ( 'NONE', #8520, 0.1000000000000002554 ) ;
#413=DIRECTION ( 'NONE',  ( 1.000000000000000000, 0.000000000000000000, 0.000000000000000000 ) ) ;
#415=CIRCLE ( 'NONE', #5701, 0.1000000000000002554 ) ;
#420=CIRCLE ( 'NONE', #2878, 6.750000000000007994 ) ;
#427=CIRCLE ( 'NONE', #1301, 5.525000000000006573 ) ;
#431=CARTESIAN_POINT ( 'NONE',  ( 1.400000000000001910, -1.415534356397074737E-16, -5.100000000000006750 ) ) ;
#457=VERTEX_POINT ( 'NONE', #3077 ) ;
#477=ORIENTED_EDGE ( 'NONE', *, *, #2129, .T. ) ;
#488=ORIENTED_EDGE ( 'NONE', *, *, #2343, .T. ) ;
#515=ORIENTED_EDGE ( 'NONE', *, *, #3176, .F. ) ;
#517=CARTESIAN_POINT ( 'NONE',  ( 1.399999999999998579, 0.000000000000000000, 0.000000000000000000 ) ) ;
#519=DIRECTION ( 'NONE',  ( 0.000000000000000000, 1.502202555303639631E-16, 1.000000000000000000 ) ) ;
#550=ORIENTED_EDGE ( 'NONE', *, *, #3080, .T. ) ;
#553=DIRECTION ( 'NONE',  ( 1.000000000000000000, 0.000000000000000000, 0.000000000000000000 ) ) ;
#561=VECTOR ( 'NONE', #1063, 1000.000000000000000 ) ;
#578=CARTESIAN_POINT ( 'NONE',  ( 1.500000000000001332, -2.053912595556539452E-16, -7.400000000000007461 ) ) ;
#579=ORIENTED_EDGE ( 'NONE', *, *, #4051, .T. ) ;
#581=AXIS2_PLACEMENT_3D ( 'NONE', #6035, #5977, #10168 ) ;
#602=ADVANCED_FACE ( 'NONE', ( #6052 ), #6853, .T. ) ;
#610=CARTESIAN_POINT ( 'NONE',  ( -20.63749999999999929, 0.000000000000000000, 0.000000000000000000 ) ) ;
#619=ORIENTED_EDGE ( 'NONE', *, *, #10120, .T. ) ;
#631=VERTEX_POINT ( 'NONE', #10241 ) ;
#638=DIRECTION ( 'NONE',  ( 0.000000000000000000, -2.775557561562891351E-17, -1.000000000000000000 ) ) ;
#666=CARTESIAN_POINT ( 'NONE',  ( -20.63749999999999929, 8.637664692995951295E-16, 5.750000000000006217 ) ) ;
#670=DIRECTION ( 'NONE',  ( 0.000000000000000000, -2.775557561562888270E-17, -1.000000000000000000 ) ) ;
#687=CARTESIAN_POINT ( 'NONE',  ( -1.400000000000001910, -1.415534356397074737E-16, -5.100000000000006750 ) ) ;
#702=SURFACE_STYLE_FILL_AREA ( #3978 ) ;
#707=PRODUCT_CONTEXT ( 'NONE', #3857, 'mechanical' ) ;
#744=CARTESIAN_POINT ( 'NONE',  ( 0.000000000000000000, 5.919319018694160373E-16, -6.250000000000007105 ) ) ;
#749=AXIS2_PLACEMENT_3D ( 'NONE', #4855, #8981, #8097 ) ;
#756=CARTESIAN_POINT ( 'NONE',  ( 1.400000000000001910, 0.000000000000000000, 0.000000000000000000 ) ) ;
#774=ADVANCED_FACE ( 'NONE', ( #4722 ), #8028, .F. ) ;
#789=DIRECTION ( 'NONE',  ( 1.000000000000000000, 0.000000000000000000, 0.000000000000000000 ) ) ;
#813=CARTESIAN_POINT ( 'NONE',  ( -0.5590169943749458970, 8.637664692995941434E-16, 5.750000000000000000 ) ) ;
#823=FACE_OUTER_BOUND ( 'NONE', #9392, .T. ) ;
#856=VERTEX_POINT ( 'NONE', #4830 ) ;
#860=AXIS2_PLACEMENT_3D ( 'NONE', #2560, #5955, #5987 ) ;
#899=TOROIDAL_SURFACE ( 'NONE', #7083, 6.250000000000000000, 0.7500000000000000000 ) ;
#948=CIRCLE ( 'NONE', #4114, 5.750000000000006217 ) ;
#958=( NAMED_UNIT ( * ) PLANE_ANGLE_UNIT ( ) SI_UNIT ( $, .RADIAN. ) );
#982=CARTESIAN_POINT ( 'NONE',  ( 1.500000000000001332, 0.000000000000000000, 0.000000000000000000 ) ) ;
#1010=SHAPE_REPRESENTATION_RELATIONSHIP ( 'NONE' , 'NONE' ,  #7612, #4934 ) ;
#1061=DIRECTION ( 'NONE',  ( 1.000000000000000000, 0.000000000000000000, 0.000000000000000000 ) ) ;
#1063=DIRECTION ( 'NONE',  ( 1.000000000000000000, 0.000000000000000000, 0.000000000000000000 ) ) ;
#1084=TOROIDAL_SURFACE ( 'NONE', #7782, 7.399999999999999467, 0.1000000000000000472 ) ;
#1085=DIRECTION ( 'NONE',  ( 0.000000000000000000, 2.775557561562888270E-17, 1.000000000000000000 ) ) ;
#1111=ORIENTED_EDGE ( 'NONE', *, *, #7014, .F. ) ;
#1141=AXIS2_PLACEMENT_3D ( 'NONE', #1158, #7987, #9693 ) ;
#1158=CARTESIAN_POINT ( 'NONE',  ( -0.1920286436967143240, 0.000000000000000000, 0.000000000000000000 ) ) ;
#1164=ORIENTED_EDGE ( 'NONE', *, *, #4969, .T. ) ;
#1177=FACE_BOUND ( 'NONE', #4966, .T. ) ;
#1191=CARTESIAN_POINT ( 'NONE',  ( -20.63749999999999929, 0.000000000000000000, 0.000000000000000000 ) ) ;
#1198=ORIENTED_EDGE ( 'NONE', *, *, #94, .T. ) ;
#1203=EDGE_CURVE ( 'NONE', #9038, #4797, #2952, .T. ) ;
#1218=AXIS2_PLACEMENT_3D ( 'NONE', #4887, #10853, #1618 ) ;
#1221=AXIS2_PLACEMENT_3D ( 'NONE', #4453, #8456, #2645 ) ;
#1234=CARTESIAN_POINT ( 'NONE',  ( -0.1920286436967143240, 0.000000000000000000, 0.000000000000000000 ) ) ;
#1253=EDGE_CURVE ( 'NONE', #6230, #9320, #6686, .T. ) ;
#1257=VECTOR ( 'NONE', #4808, 1000.000000000000000 ) ;
#1278=AXIS2_PLACEMENT_3D ( 'NONE', #6452, #2234, #9803 ) ;
#1285=ORIENTED_EDGE ( 'NONE', *, *, #1522, .F. ) ;
#1290=DIRECTION ( 'NONE',  ( -1.000000000000000000, -0.000000000000000000, -0.000000000000000000 ) ) ;
#1301=AXIS2_PLACEMENT_3D ( 'NONE', #9916, #4746, #7268 ) ;
#1304=FACE_OUTER_BOUND ( 'NONE', #10765, .T. ) ;
#1357=ORIENTED_EDGE ( 'NONE', *, *, #1253, .T. ) ;
#1366=ORIENTED_EDGE ( 'NONE', *, *, #3618, .F. ) ;
#1377=ADVANCED_FACE ( 'NONE', ( #8628 ), #5102, .F. ) ;
#1392=EDGE_LOOP ( 'NONE', ( #5015, #7159, #4615, #6449 ) ) ;
#1394=VERTEX_POINT ( 'NONE', #10347 ) ;
#1401=FACE_OUTER_BOUND ( 'NONE', #2174, .T. ) ;
#1417=ORIENTED_EDGE ( 'NONE', *, *, #2410, .T. ) ;
#1435=PLANE ( 'NONE',  #3146 ) ;
#1453=CIRCLE ( 'NONE', #2154, 6.975000000000008527 ) ;
#1455=EDGE_CURVE ( 'NONE', #7330, #4112, #10426, .T. ) ;
#1477=CARTESIAN_POINT ( 'NONE',  ( 1.500000000000001332, 7.400000000000008349, 2.168404344971008868E-16 ) ) ;
#1482=CYLINDRICAL_SURFACE ( 'NONE', #9492, 6.975000000000008527 ) ;
#1498=FACE_BOUND ( 'NONE', #8807, .T. ) ;
#1518=CARTESIAN_POINT ( 'NONE',  ( -20.63749999999999574, 1.047786282324291578E-15, 6.975000000000008527 ) ) ;
#1522=EDGE_CURVE ( 'NONE', #10165, #9038, #6375, .T. ) ;
#1527=PRESENTATION_STYLE_ASSIGNMENT (( #4081 ) ) ;
#1537=TOROIDAL_SURFACE ( 'NONE', #8419, 5.100000000000000533, 0.1000000000000001582 ) ;
#1568=PRODUCT_DEFINITION_FORMATION_WITH_SPECIFIED_SOURCE ( 'ANY', '', #10587, .NOT_KNOWN. ) ;
#1577=EDGE_LOOP ( 'NONE', ( #2318, #1198, #4126, #7882 ) ) ;
#1578=CIRCLE ( 'NONE', #7405, 5.750000000000006217 ) ;
#1581=VECTOR ( 'NONE', #8736, 1000.000000000000000 ) ;
#1603=FACE_OUTER_BOUND ( 'NONE', #2945, .T. ) ;
#1607=DIRECTION ( 'NONE',  ( 0.000000000000000000, -2.775557561562887961E-17, -1.000000000000000000 ) ) ;
#1616=AXIS2_PLACEMENT_3D ( 'NONE', #8394, #9070, #670 ) ;
#1618=DIRECTION ( 'NONE',  ( 0.000000000000000000, -2.775557561562887961E-17, -1.000000000000000000 ) ) ;
#1625=DIRECTION ( 'NONE',  ( 0.000000000000000000, 1.502202555303639631E-16, 1.000000000000000000 ) ) ;
#1631=CIRCLE ( 'NONE', #10466, 0.1000000000000002554 ) ;
#1648=DIRECTION ( 'NONE',  ( 0.000000000000000000, -2.775557561562888270E-17, -1.000000000000000000 ) ) ;
#1657=EDGE_CURVE ( 'NONE', #3713, #856, #7957, .T. ) ;
#1664=CARTESIAN_POINT ( 'NONE',  ( -1.499999999999997780, 6.975000000000008527, 6.505213034913026604E-16 ) ) ;
#1699=CARTESIAN_POINT ( 'NONE',  ( 0.000000000000000000, 0.000000000000000000, 0.000000000000000000 ) ) ;
#1713=DIRECTION ( 'NONE',  ( 0.000000000000000000, -2.775557561562888270E-17, -1.000000000000000000 ) ) ;
#1722=ORIENTED_EDGE ( 'NONE', *, *, #1203, .F. ) ;
#1738=EDGE_LOOP ( 'NONE', ( #1366, #5245 ) ) ;
#1756=DIRECTION ( 'NONE',  ( 0.000000000000000000, -2.775557561562888270E-17, -1.000000000000000000 ) ) ;
#1765=VERTEX_POINT ( 'NONE', #3843 ) ;
#1774=CARTESIAN_POINT ( 'NONE',  ( 1.400000000000001910, 0.000000000000000000, 0.000000000000000000 ) ) ;
#1777=DIRECTION ( 'NONE',  ( 1.000000000000000000, 0.000000000000000000, 0.000000000000000000 ) ) ;
#1814=EDGE_CURVE ( 'NONE', #2818, #8744, #9749, .T. ) ;
#1823=CIRCLE ( 'NONE', #7994, 5.100000000000006750 ) ;
#1838=CARTESIAN_POINT ( 'NONE',  ( -20.63749999999999574, 0.000000000000000000, 0.000000000000000000 ) ) ;
#1840=AXIS2_PLACEMENT_3D ( 'NONE', #2183, #9848, #5666 ) ;
#1868=DIRECTION ( 'NONE',  ( 0.000000000000000000, -2.775557561562887961E-17, -1.000000000000000000 ) ) ;
#1904=CARTESIAN_POINT ( 'NONE',  ( 0.000000000000000000, 0.000000000000000000, 0.000000000000000000 ) ) ;
#1948=( NAMED_UNIT ( * ) SI_UNIT ( $, .STERADIAN. ) SOLID_ANGLE_UNIT ( ) );
#1962=DIRECTION ( 'NONE',  ( 1.000000000000000000, 0.000000000000000000, 0.000000000000000000 ) ) ;
#1998=CIRCLE ( 'NONE', #8154, 0.1000000000000002554 ) ;
#2008=CARTESIAN_POINT ( 'NONE',  ( -1.500000000000001332, 1.119140903701213403E-15, 7.399999999999999467 ) ) ;
#2009=CIRCLE ( 'NONE', #7445, 6.750000000000007994 ) ;
#2034=DIRECTION ( 'NONE',  ( 0.000000000000000000, 2.775557561562888270E-17, 1.000000000000000000 ) ) ;
#2044=CARTESIAN_POINT ( 'NONE',  ( 1.400000000000001910, 0.000000000000000000, 0.000000000000000000 ) ) ;
#2051=EDGE_LOOP ( 'NONE', ( #8901, #2903, #8334, #2831 ) ) ;
#2080=EDGE_LOOP ( 'NONE', ( #9339, #4954, #8365, #2306 ) ) ;
#2114=CIRCLE ( 'NONE', #2283, 7.500000000000007994 ) ;
#2120=AXIS2_PLACEMENT_3D ( 'NONE', #10162, #5971, #6093 ) ;
#2128=ORIENTED_EDGE ( 'NONE', *, *, #5183, .F. ) ;
#2129=EDGE_CURVE ( 'NONE', #9320, #9464, #4252, .T. ) ;
#2154=AXIS2_PLACEMENT_3D ( 'NONE', #10922, #10869, #3384 ) ;
#2158=DIRECTION ( 'NONE',  ( 1.000000000000000000, 0.000000000000000000, 0.000000000000000000 ) ) ;
#2174=EDGE_LOOP ( 'NONE', ( #9350, #7352, #1357, #4979 ) ) ;
#2178=CARTESIAN_POINT ( 'NONE',  ( 0.000000000000000000, 0.000000000000000000, 0.000000000000000000 ) ) ;
#2183=CARTESIAN_POINT ( 'NONE',  ( -1.399999999999998579, 0.000000000000000000, 0.000000000000000000 ) ) ;
#2212=DIRECTION ( 'NONE',  ( 0.000000000000000000, -2.775557561562888270E-17, -1.000000000000000000 ) ) ;
#2219=EDGE_CURVE ( 'NONE', #8585, #7956, #9533, .T. ) ;
#2234=DIRECTION ( 'NONE',  ( 0.000000000000000000, 1.000000000000000000, -1.502202555303642096E-16 ) ) ;
#2273=EDGE_LOOP ( 'NONE', ( #10863, #5875, #10499, #2559 ) ) ;
#2275=ORIENTED_EDGE ( 'NONE', *, *, #8022, .F. ) ;
#2283=AXIS2_PLACEMENT_3D ( 'NONE', #6812, #789, #8395 ) ;
#2297=TOROIDAL_SURFACE ( 'NONE', #373, 7.399999999999999467, 0.1000000000000000472 ) ;
#2306=ORIENTED_EDGE ( 'NONE', *, *, #1253, .F. ) ;
#2318=ORIENTED_EDGE ( 'NONE', *, *, #3700, .F. ) ;
#2335=CIRCLE ( 'NONE', #6067, 5.100000000000006750 ) ;
#2337=CARTESIAN_POINT ( 'NONE',  ( 0.000000000000000000, 5.919319018694160373E-16, -6.250000000000007105 ) ) ;
#2339=AXIS2_PLACEMENT_3D ( 'NONE', #687, #5824, #5766 ) ;
#2343=EDGE_CURVE ( 'NONE', #9464, #9320, #2114, .T. ) ;
#2355=DIRECTION ( 'NONE',  ( 0.000000000000000000, -2.775557561562888270E-17, -1.000000000000000000 ) ) ;
#2372=CARTESIAN_POINT ( 'NONE',  ( 1.399999999999998579, 0.000000000000000000, 0.000000000000000000 ) ) ;
#2377=CARTESIAN_POINT ( 'NONE',  ( -1.500000000000001332, 8.637664692995941434E-16, 5.750000000000000000 ) ) ;
#2389=DIRECTION ( 'NONE',  ( 1.000000000000000000, 0.000000000000000000, 0.000000000000000000 ) ) ;
#2396=ORIENTED_EDGE ( 'NONE', *, *, #9822, .F. ) ;
#2400=DIRECTION ( 'NONE',  ( 0.000000000000000000, -2.775557561562888270E-17, -1.000000000000000000 ) ) ;
#2404=( NAMED_UNIT ( * ) PLANE_ANGLE_UNIT ( ) SI_UNIT ( $, .RADIAN. ) );
#2406=EDGE_CURVE ( 'NONE', #7146, #9698, #6523, .T. ) ;
#2407=VERTEX_POINT ( 'NONE', #2377 ) ;
#2409=SHAPE_DEFINITION_REPRESENTATION ( #7944, #7612 ) ;
#2410=EDGE_CURVE ( 'NONE', #7146, #3515, #180, .T. ) ;
#2442=DIRECTION ( 'NONE',  ( 0.000000000000000000, 1.000000000000000000, 9.470910429910644418E-17 ) ) ;
#2445=ORIENTED_EDGE ( 'NONE', *, *, #8262, .F. ) ;
#2456=ORIENTED_EDGE ( 'NONE', *, *, #3587, .F. ) ;
#2463=CARTESIAN_POINT ( 'NONE',  ( -20.63749999999999574, 0.000000000000000000, 0.000000000000000000 ) ) ;
#2476=CARTESIAN_POINT ( 'NONE',  ( 1.500000000000001332, 0.000000000000000000, 0.000000000000000000 ) ) ;
#2491=AXIS2_PLACEMENT_3D ( 'NONE', #9489, #6292, #7894 ) ;
#2510=DIRECTION ( 'NONE',  ( 1.000000000000000000, 0.000000000000000000, 0.000000000000000000 ) ) ;
#2525=DIRECTION ( 'NONE',  ( 0.000000000000000000, -2.775557561562888270E-17, -1.000000000000000000 ) ) ;
#2528=ORIENTED_EDGE ( 'NONE', *, *, #7210, .F. ) ;
#2559=ORIENTED_EDGE ( 'NONE', *, *, #6320, .F. ) ;
#2560=CARTESIAN_POINT ( 'NONE',  ( -1.399999999999998579, -2.053912595556539452E-16, -7.400000000000007461 ) ) ;
#2569=FACE_OUTER_BOUND ( 'NONE', #4759, .T. ) ;
#2587=AXIS2_PLACEMENT_3D ( 'NONE', #1774, #3529, #6805 ) ;
#2612=CARTESIAN_POINT ( 'NONE',  ( 1.500000000000001332, -1.533495552763497570E-16, -5.525000000000006573 ) ) ;
#2638=( LENGTH_UNIT ( ) NAMED_UNIT ( * ) SI_UNIT ( .MILLI., .METRE. ) );
#2645=DIRECTION ( 'NONE',  ( 0.000000000000000000, -2.775557561562888270E-17, -1.000000000000000000 ) ) ;
#2669=ORIENTED_EDGE ( 'NONE', *, *, #1657, .F. ) ;
#2716=DIRECTION ( 'NONE',  ( 0.000000000000000000, -2.775557561562887961E-17, -1.000000000000000000 ) ) ;
#2722=EDGE_CURVE ( 'NONE', #8620, #7956, #5439, .T. ) ;
#2778=DIRECTION ( 'NONE',  ( 1.000000000000000000, 0.000000000000000000, 0.000000000000000000 ) ) ;
#2789=VERTEX_POINT ( 'NONE', #3087 ) ;
#2790=DIRECTION ( 'NONE',  ( 0.000000000000000000, 2.775557561562888270E-17, 1.000000000000000000 ) ) ;
#2802=LINE ( 'NONE', #6204, #1581 ) ;
#2809=SURFACE_STYLE_FILL_AREA ( #5155 ) ;
#2818=VERTEX_POINT ( 'NONE', #3512 ) ;
#2831=ORIENTED_EDGE ( 'NONE', *, *, #5771, .T. ) ;
#2878=AXIS2_PLACEMENT_3D ( 'NONE', #982, #10255, #9192 ) ;
#2880=ADVANCED_FACE ( 'NONE', ( #9881 ), #1084, .T. ) ;
#2888=ADVANCED_FACE ( 'NONE', ( #6632 ), #10717, .T. ) ;
#2894=ORIENTED_EDGE ( 'NONE', *, *, #10331, .F. ) ;
#2903=ORIENTED_EDGE ( 'NONE', *, *, #3124, .F. ) ;
#2909=DIRECTION ( 'NONE',  ( 1.000000000000000000, 0.000000000000000000, 0.000000000000000000 ) ) ;
#2942=VERTEX_POINT ( 'NONE', #8122 ) ;
#2945=EDGE_LOOP ( 'NONE', ( #515, #488, #82, #2456 ) ) ;
#2952=CIRCLE ( 'NONE', #5794, 5.525000000000006573 ) ;
#2990=DIRECTION ( 'NONE',  ( 0.000000000000000000, 1.000000000000000000, -1.502202555303642096E-16 ) ) ;
#2993=ADVANCED_FACE ( 'NONE', ( #9005 ), #10671, .T. ) ;
#3008=ORIENTED_EDGE ( 'NONE', *, *, #8939, .T. ) ;
#3066=EDGE_CURVE ( 'NONE', #5286, #1765, #9349, .T. ) ;
#3077=CARTESIAN_POINT ( 'NONE',  ( 1.400000000000001910, -1.387778780781445676E-16, -5.000000000000005329 ) ) ;
#3080=EDGE_CURVE ( 'NONE', #4640, #8585, #9217, .T. ) ;
#3087=CARTESIAN_POINT ( 'NONE',  ( -1.500000000000001776, 7.661233032048582725E-16, 5.100000000000006750 ) ) ;
#3094=CARTESIAN_POINT ( 'NONE',  ( -1.500000000000001332, 0.000000000000000000, 0.000000000000000000 ) ) ;
#3099=CARTESIAN_POINT ( 'NONE',  ( 1.400000000000001910, 7.586122904283394383E-16, 5.000000000000000000 ) ) ;
#3107=FACE_OUTER_BOUND ( 'NONE', #8921, .T. ) ;
#3117=CARTESIAN_POINT ( 'NONE',  ( -0.1920286436967143240, 6.605960024862680574E-16, -6.975000000000007638 ) ) ;
#3121=ORIENTED_EDGE ( 'NONE', *, *, #5395, .F. ) ;
#3124=EDGE_CURVE ( 'NONE', #1765, #5286, #6906, .T. ) ;
#3134=CARTESIAN_POINT ( 'NONE',  ( 1.500000000000001776, 7.661233032048582725E-16, 5.100000000000006750 ) ) ;
#3139=ADVANCED_FACE ( 'NONE', ( #8557, #4436 ), #9453, .T. ) ;
#3146=AXIS2_PLACEMENT_3D ( 'NONE', #1664, #6636, #6477 ) ;
#3167=AXIS2_PLACEMENT_3D ( 'NONE', #3094, #8142, #5309 ) ;
#3176=EDGE_CURVE ( 'NONE', #9464, #3515, #2802, .T. ) ;
#3192=CIRCLE ( 'NONE', #8864, 7.400000000000007461 ) ;
#3215=TOROIDAL_SURFACE ( 'NONE', #1840, 7.399999999999999467, 0.1000000000000000472 ) ;
#3231=EDGE_LOOP ( 'NONE', ( #2528, #2669 ) ) ;
#3240=CARTESIAN_POINT ( 'NONE',  ( 1.399999999999998579, -2.053912595556539452E-16, -7.400000000000007461 ) ) ;
#3268=CARTESIAN_POINT ( 'NONE',  ( 1.399999999999998579, 1.111629890924696344E-15, 7.400000000000007461 ) ) ;
#3282=EDGE_CURVE ( 'NONE', #8620, #4640, #6540, .T. ) ;
#3311=DIRECTION ( 'NONE',  ( -1.000000000000000000, 0.000000000000000000, 0.000000000000000000 ) ) ;
#3318=ORIENTED_EDGE ( 'NONE', *, *, #9879, .T. ) ;
#3353=ORIENTED_EDGE ( 'NONE', *, *, #9892, .T. ) ;
#3371=TOROIDAL_SURFACE ( 'NONE', #7112, 6.250000000000000000, 0.7500000000000000000 ) ;
#3384=DIRECTION ( 'NONE',  ( 0.000000000000000000, -2.775557561562888270E-17, -1.000000000000000000 ) ) ;
#3385=EDGE_CURVE ( 'NONE', #9320, #7146, #6460, .T. ) ;
#3391=AXIS2_PLACEMENT_3D ( 'NONE', #2044, #4598, #3748 ) ;
#3431=DIRECTION ( 'NONE',  ( 0.000000000000000000, 0.000000000000000000, 1.000000000000000000 ) ) ;
#3437=DIRECTION ( 'NONE',  ( 0.000000000000000000, -9.470910429910653047E-17, 1.000000000000000000 ) ) ;
#3438=ORIENTED_EDGE ( 'NONE', *, *, #5204, .T. ) ;
#3506=DIRECTION ( 'NONE',  ( 1.000000000000000000, 0.000000000000000000, 0.000000000000000000 ) ) ;
#3508=DIRECTION ( 'NONE',  ( 0.000000000000000000, -2.775557561562888270E-17, -1.000000000000000000 ) ) ;
#3512=CARTESIAN_POINT ( 'NONE',  ( -1.500000000000001332, -1.595945597898662527E-16, -5.750000000000006217 ) ) ;
#3515=VERTEX_POINT ( 'NONE', #3578 ) ;
#3529=DIRECTION ( 'NONE',  ( 1.000000000000000000, 0.000000000000000000, 0.000000000000000000 ) ) ;
#3542=ADVANCED_FACE ( 'NONE', ( #1304 ), #899, .T. ) ;
#3550=ADVANCED_FACE ( 'NONE', ( #4688 ), #2297, .T. ) ;
#3562=DIRECTION ( 'NONE',  ( 1.000000000000000000, 0.000000000000000000, 0.000000000000000000 ) ) ;
#3563=AXIS2_PLACEMENT_3D ( 'NONE', #7962, #5424, #167 ) ;
#3578=CARTESIAN_POINT ( 'NONE',  ( 1.399999999999998579, 1.126651916477731646E-15, 7.500000000000000000 ) ) ;
#3587=EDGE_CURVE ( 'NONE', #3515, #7146, #9700, .T. ) ;
#3593=LINE ( 'NONE', #6145, #561 ) ;
#3618=EDGE_CURVE ( 'NONE', #6230, #7276, #4254, .T. ) ;
#3651=( LENGTH_UNIT ( ) NAMED_UNIT ( * ) SI_UNIT ( .MILLI., .METRE. ) );
#3660=MECHANICAL_DESIGN_GEOMETRIC_PRESENTATION_REPRESENTATION('',(#7351),#310);
#3662=CARTESIAN_POINT ( 'NONE',  ( 0.5590169943749494497, 0.000000000000000000, 0.000000000000000000 ) ) ;
#3685=CARTESIAN_POINT ( 'NONE',  ( 1.500000000000001332, 0.000000000000000000, 0.000000000000000000 ) ) ;
#3697=ORIENTED_EDGE ( 'NONE', *, *, #7106, .F. ) ;
#3700=EDGE_CURVE ( 'NONE', #2407, #6845, #9067, .T. ) ;
#3707=ORIENTED_EDGE ( 'NONE', *, *, #3080, .F. ) ;
#3713=VERTEX_POINT ( 'NONE', #3134 ) ;
#3714=VECTOR ( 'NONE', #3865, 1000.000000000000000 ) ;
#3742=ORIENTED_EDGE ( 'NONE', *, *, #9879, .F. ) ;
#3748=DIRECTION ( 'NONE',  ( 0.000000000000000000, -2.775557561562887961E-17, -1.000000000000000000 ) ) ;
#3751=AXIS2_PLACEMENT_3D ( 'NONE', #8765, #148, #3508 ) ;
#3756=ADVANCED_FACE ( 'NONE', ( #1498, #4931 ), #1435, .T. ) ;
#3763=EDGE_LOOP ( 'NONE', ( #9605, #8045 ) ) ;
#3771=TOROIDAL_SURFACE ( 'NONE', #581, 5.100000000000000533, 0.1000000000000001582 ) ;
#3843=CARTESIAN_POINT ( 'NONE',  ( -1.400000000000001910, -1.387778780781445676E-16, -5.000000000000005329 ) ) ;
#3857=APPLICATION_CONTEXT ( 'automotive_design' ) ;
#3865=DIRECTION ( 'NONE',  ( 1.000000000000000000, 0.000000000000000000, 0.000000000000000000 ) ) ;
#3884=VECTOR ( 'NONE', #6324, 1000.000000000000000 ) ;
#3889=ORIENTED_EDGE ( 'NONE', *, *, #5183, .T. ) ;
#3894=DIRECTION ( 'NONE',  ( 1.000000000000000000, 0.000000000000000000, 0.000000000000000000 ) ) ;
#3917=ORIENTED_EDGE ( 'NONE', *, *, #6870, .T. ) ;
#3922=ORIENTED_EDGE ( 'NONE', *, *, #5204, .F. ) ;
#3937=DIRECTION ( 'NONE',  ( 0.000000000000000000, -2.775557561562888270E-17, -1.000000000000000000 ) ) ;
#3978=FILL_AREA_STYLE ('',( #10036 ) ) ;
#3987=ORIENTED_EDGE ( 'NONE', *, *, #2722, .T. ) ;
#4000=EDGE_LOOP ( 'NONE', ( #10494, #2128, #6033, #9987 ) ) ;
#4006=DIRECTION ( 'NONE',  ( 0.000000000000000000, -2.775557561562888270E-17, -1.000000000000000000 ) ) ;
#4011=EDGE_LOOP ( 'NONE', ( #8912, #5018, #8397, #3121 ) ) ;
#4022=FACE_BOUND ( 'NONE', #4780, .T. ) ;
#4030=EDGE_CURVE ( 'NONE', #4797, #9038, #4068, .T. ) ;
#4046=DIRECTION ( 'NONE',  ( 1.000000000000000000, 0.000000000000000000, 0.000000000000000000 ) ) ;
#4051=EDGE_CURVE ( 'NONE', #5286, #9729, #7141, .T. ) ;
#4066=EDGE_LOOP ( 'NONE', ( #6705, #9615, #7809, #4896 ) ) ;
#4068=CIRCLE ( 'NONE', #9348, 5.525000000000006573 ) ;
#4081=SURFACE_STYLE_USAGE ( .BOTH. , #5787 ) ;
#4093=EDGE_CURVE ( 'NONE', #631, #4112, #8056, .T. ) ;
#4108=AXIS2_PLACEMENT_3D ( 'NONE', #9428, #2778, #6959 ) ;
#4112=VERTEX_POINT ( 'NONE', #3117 ) ;
#4114=AXIS2_PLACEMENT_3D ( 'NONE', #5095, #5922, #9271 ) ;
#4117=AXIS2_PLACEMENT_3D ( 'NONE', #9448, #8494, #5964 ) ;
#4126=ORIENTED_EDGE ( 'NONE', *, *, #1814, .T. ) ;
#4127=ORIENTED_EDGE ( 'NONE', *, *, #4903, .T. ) ;
#4142=DIRECTION ( 'NONE',  ( 0.000000000000000000, 2.775557561562888270E-17, 1.000000000000000000 ) ) ;
#4183=ORIENTED_EDGE ( 'NONE', *, *, #1455, .T. ) ;
#4244=DIRECTION ( 'NONE',  ( 1.000000000000000000, 0.000000000000000000, 0.000000000000000000 ) ) ;
#4252=CIRCLE ( 'NONE', #10431, 7.500000000000007994 ) ;
#4254=CIRCLE ( 'NONE', #3167, 7.400000000000007461 ) ;
#4257=DIRECTION ( 'NONE',  ( 1.000000000000000000, 0.000000000000000000, 0.000000000000000000 ) ) ;
#4264=CARTESIAN_POINT ( 'NONE',  ( 1.500000000000001332, 0.000000000000000000, 0.000000000000000000 ) ) ;
#4273=DIRECTION ( 'NONE',  ( 1.000000000000000000, -0.000000000000000000, -0.000000000000000000 ) ) ;
#4304=VECTOR ( 'NONE', #8982, 1000.000000000000000 ) ;
#4313=EDGE_CURVE ( 'NONE', #2818, #2407, #1578, .T. ) ;
#4319=CYLINDRICAL_SURFACE ( 'NONE', #4373, 5.750000000000006217 ) ;
#4340=CARTESIAN_POINT ( 'NONE',  ( -1.399999999999998579, 0.000000000000000000, 0.000000000000000000 ) ) ;
#4372=CARTESIAN_POINT ( 'NONE',  ( -20.63749999999999574, 1.013986724829959586E-15, 6.750000000000007994 ) ) ;
#4373=AXIS2_PLACEMENT_3D ( 'NONE', #109, #8676, #6980 ) ;
#4378=SURFACE_STYLE_USAGE ( .BOTH. , #4509 ) ;
#4407=VERTEX_POINT ( 'NONE', #7789 ) ;
#4432=PRODUCT_DEFINITION ( 'UNKNOWN', '', #1568, #4942 ) ;
#4436=FACE_BOUND ( 'NONE', #3231, .T. ) ;
#4453=CARTESIAN_POINT ( 'NONE',  ( -20.63749999999999929, 0.000000000000000000, 0.000000000000000000 ) ) ;
#4476=EDGE_LOOP ( 'NONE', ( #3707, #10915, #3987, #4127 ) ) ;
#4486=CIRCLE ( 'NONE', #6945, 6.975000000000008527 ) ;
#4488=AXIS2_PLACEMENT_3D ( 'NONE', #9407, #1962, #7874 ) ;
#4494=CARTESIAN_POINT ( 'NONE',  ( 0.5590169943749494497, 1.873501354054951415E-16, 6.750000000000007105 ) ) ;
#4509=SURFACE_SIDE_STYLE ('',( #2809 ) ) ;
#4523=CARTESIAN_POINT ( 'NONE',  ( 0.000000000000000000, 0.000000000000000000, 0.000000000000000000 ) ) ;
#4564=COLOUR_RGB ( '', 0.72549020, 0.75294118, 0.79215686) ;
#4587=DIRECTION ( 'NONE',  ( 1.000000000000000000, 0.000000000000000000, 0.000000000000000000 ) ) ;
#4598=DIRECTION ( 'NONE',  ( 1.000000000000000000, 0.000000000000000000, 0.000000000000000000 ) ) ;
#4607=FACE_OUTER_BOUND ( 'NONE', #9788, .T. ) ;
#4615=ORIENTED_EDGE ( 'NONE', *, *, #4994, .F. ) ;
#4640=VERTEX_POINT ( 'NONE', #4494 ) ;
#4664=EDGE_LOOP ( 'NONE', ( #10122, #579, #7471, #123 ) ) ;
#4669=EDGE_CURVE ( 'NONE', #4407, #7330, #6613, .T. ) ;
#4688=FACE_OUTER_BOUND ( 'NONE', #6674, .T. ) ;
#4704=DIRECTION ( 'NONE',  ( 0.000000000000000000, 2.775557561562887961E-17, 1.000000000000000000 ) ) ;
#4714=EDGE_CURVE ( 'NONE', #2942, #10165, #427, .T. ) ;
#4722=FACE_OUTER_BOUND ( 'NONE', #4664, .T. ) ;
#4723=CARTESIAN_POINT ( 'NONE',  ( -20.63749999999999574, -1.873501354054951662E-16, -6.750000000000007994 ) ) ;
#4727=( GEOMETRIC_REPRESENTATION_CONTEXT ( 3 ) GLOBAL_UNCERTAINTY_ASSIGNED_CONTEXT ( ( #8138 ) ) GLOBAL_UNIT_ASSIGNED_CONTEXT ( ( #2638, #9458, #1948 ) ) REPRESENTATION_CONTEXT ( 'NONE', 'WORKASPACE' ) );
#4746=DIRECTION ( 'NONE',  ( -1.000000000000000000, 0.000000000000000000, 0.000000000000000000 ) ) ;
#4759=EDGE_LOOP ( 'NONE', ( #1285, #7365, #6780, #1722 ) ) ;
#4765=AXIS2_PLACEMENT_3D ( 'NONE', #4264, #9226, #1607 ) ;
#4767=CARTESIAN_POINT ( 'NONE',  ( -20.63749999999999574, 0.000000000000000000, 0.000000000000000000 ) ) ;
#4780=EDGE_LOOP ( 'NONE', ( #8114, #6630 ) ) ;
#4797=VERTEX_POINT ( 'NONE', #2612 ) ;
#4799=DIRECTION ( 'NONE',  ( 0.000000000000000000, -1.000000000000000000, 2.775557561562888270E-17 ) ) ;
#4803=DIRECTION ( 'NONE',  ( 1.000000000000000000, 0.000000000000000000, 0.000000000000000000 ) ) ;
#4804=PLANE ( 'NONE',  #4989 ) ;
#4808=DIRECTION ( 'NONE',  ( 1.000000000000000000, 0.000000000000000000, 0.000000000000000000 ) ) ;
#4817=CIRCLE ( 'NONE', #2491, 0.7499999999999997780 ) ;
#4830=CARTESIAN_POINT ( 'NONE',  ( 1.500000000000001776, -1.415534356397074737E-16, -5.100000000000006750 ) ) ;
#4855=CARTESIAN_POINT ( 'NONE',  ( -20.63749999999999574, 0.000000000000000000, 0.000000000000000000 ) ) ;
#4871=DIRECTION ( 'NONE',  ( 0.000000000000000000, -2.775557561562887961E-17, -1.000000000000000000 ) ) ;
#4887=CARTESIAN_POINT ( 'NONE',  ( 0.000000000000000000, 1.734723475976807094E-16, 6.250000000000007105 ) ) ;
#4896=ORIENTED_EDGE ( 'NONE', *, *, #6654, .F. ) ;
#4898=MECHANICAL_DESIGN_GEOMETRIC_PRESENTATION_REPRESENTATION('',(#10192),#9826);
#4903=EDGE_CURVE ( 'NONE', #7956, #8585, #420, .T. ) ;
#4912=( LENGTH_UNIT ( ) NAMED_UNIT ( * ) SI_UNIT ( .MILLI., .METRE. ) );
#4921=ADVANCED_FACE ( 'NONE', ( #10420 ), #207, .T. ) ;
#4928=DIRECTION ( 'NONE',  ( 1.000000000000000000, 0.000000000000000000, 0.000000000000000000 ) ) ;
#4931=FACE_OUTER_BOUND ( 'NONE', #1738, .T. ) ;
#4934=ADVANCED_BREP_SHAPE_REPRESENTATION ( '', ( #10510, #7040 ), #4727 ) ;
#4942=PRODUCT_DEFINITION_CONTEXT ( 'detailed design', #8930, 'design' ) ;
#4954=ORIENTED_EDGE ( 'NONE', *, *, #6588, .T. ) ;
#4957=AXIS2_PLACEMENT_3D ( 'NONE', #4767, #553, #3937 ) ;
#4961=DIRECTION ( 'NONE',  ( 0.000000000000000000, 1.000000000000000000, -1.502202555303642096E-16 ) ) ;
#4963=AXIS2_PLACEMENT_3D ( 'NONE', #10496, #5467, #4704 ) ;
#4966=EDGE_LOOP ( 'NONE', ( #619, #7507 ) ) ;
#4969=EDGE_CURVE ( 'NONE', #10165, #2942, #6424, .T. ) ;
#4979=ORIENTED_EDGE ( 'NONE', *, *, #2343, .F. ) ;
#4989=AXIS2_PLACEMENT_3D ( 'NONE', #1477, #7374, #2355 ) ;
#4994=EDGE_CURVE ( 'NONE', #4112, #7330, #9224, .T. ) ;
#5000=CIRCLE ( 'NONE', #2339, 0.1000000000000002554 ) ;
#5015=ORIENTED_EDGE ( 'NONE', *, *, #6722, .F. ) ;
#5018=ORIENTED_EDGE ( 'NONE', *, *, #3066, .T. ) ;
#5080=DIRECTION ( 'NONE',  ( 0.000000000000000000, -2.775557561562888270E-17, -1.000000000000000000 ) ) ;
#5094=( NAMED_UNIT ( * ) SI_UNIT ( $, .STERADIAN. ) SOLID_ANGLE_UNIT ( ) );
#5095=CARTESIAN_POINT ( 'NONE',  ( -0.5590169943749458970, 0.000000000000000000, 0.000000000000000000 ) ) ;
#5102=CYLINDRICAL_SURFACE ( 'NONE', #1221, 5.000000000000005329 ) ;
#5126=ADVANCED_FACE ( 'NONE', ( #1401 ), #3215, .T. ) ;
#5132=AXIS2_PLACEMENT_3D ( 'NONE', #7618, #1061, #2525 ) ;
#5155=FILL_AREA_STYLE ('',( #8562 ) ) ;
#5156=CARTESIAN_POINT ( 'NONE',  ( 1.399999999999998579, -2.081668171172168513E-16, -7.500000000000007994 ) ) ;
#5179=CIRCLE ( 'NONE', #3751, 7.400000000000007461 ) ;
#5183=EDGE_CURVE ( 'NONE', #631, #4407, #4486, .T. ) ;
#5187=DIRECTION ( 'NONE',  ( 0.000000000000000000, -2.775557561562887961E-17, -1.000000000000000000 ) ) ;
#5188=CIRCLE ( 'NONE', #42, 0.7499999999999997780 ) ;
#5204=EDGE_CURVE ( 'NONE', #2942, #8620, #5188, .T. ) ;
#5205=CARTESIAN_POINT ( 'NONE',  ( 1.500000000000001332, 0.000000000000000000, 0.000000000000000000 ) ) ;
#5216=CARTESIAN_POINT ( 'NONE',  ( -1.500000000000001332, 0.000000000000000000, 0.000000000000000000 ) ) ;
#5236=CARTESIAN_POINT ( 'NONE',  ( -20.63749999999999574, 0.000000000000000000, 0.000000000000000000 ) ) ;
#5245=ORIENTED_EDGE ( 'NONE', *, *, #6186, .F. ) ;
#5286=VERTEX_POINT ( 'NONE', #10344 ) ;
#5293=FACE_OUTER_BOUND ( 'NONE', #2080, .T. ) ;
#5299=DIRECTION ( 'NONE',  ( 1.000000000000000000, 0.000000000000000000, 0.000000000000000000 ) ) ;
#5309=DIRECTION ( 'NONE',  ( 0.000000000000000000, -2.775557561562888270E-17, -1.000000000000000000 ) ) ;
#5365=TOROIDAL_SURFACE ( 'NONE', #6248, 7.399999999999999467, 0.1000000000000000472 ) ;
#5374=AXIS2_PLACEMENT_3D ( 'NONE', #2463, #8493, #10937 ) ;
#5395=EDGE_CURVE ( 'NONE', #2789, #6566, #2335, .T. ) ;
#5424=DIRECTION ( 'NONE',  ( -1.000000000000000000, 0.000000000000000000, 0.000000000000000000 ) ) ;
#5439=LINE ( 'NONE', #4723, #3884 ) ;
#5467=DIRECTION ( 'NONE',  ( 1.000000000000000000, -0.000000000000000000, -0.000000000000000000 ) ) ;
#5488=VECTOR ( 'NONE', #2158, 1000.000000000000000 ) ;
#5494=ORIENTED_EDGE ( 'NONE', *, *, #2406, .T. ) ;
#5528=CARTESIAN_POINT ( 'NONE',  ( 1.500000000000001332, 0.000000000000000000, 0.000000000000000000 ) ) ;
#5554=EDGE_LOOP ( 'NONE', ( #3742, #6982, #8728, #3008 ) ) ;
#5558=DIRECTION ( 'NONE',  ( -1.000000000000000000, 0.000000000000000000, 0.000000000000000000 ) ) ;
#5574=ADVANCED_FACE ( 'NONE', ( #2569 ), #10940, .T. ) ;
#5587=ORIENTED_EDGE ( 'NONE', *, *, #10113, .F. ) ;
#5628=EDGE_LOOP ( 'NONE', ( #477, #9641, #5804, #5892 ) ) ;
#5629=ORIENTED_EDGE ( 'NONE', *, *, #8262, .T. ) ;
#5666=DIRECTION ( 'NONE',  ( 0.000000000000000000, -2.775557561562888270E-17, -1.000000000000000000 ) ) ;
#5701=AXIS2_PLACEMENT_3D ( 'NONE', #8412, #9186, #1625 ) ;
#5708=DIRECTION ( 'NONE',  ( 0.000000000000000000, -2.775557561562891351E-17, -1.000000000000000000 ) ) ;
#5724=ADVANCED_FACE ( 'NONE', ( #10437 ), #10477, .T. ) ;
#5753=DIRECTION ( 'NONE',  ( 1.000000000000000000, 0.000000000000000000, 0.000000000000000000 ) ) ;
#5766=DIRECTION ( 'NONE',  ( 0.000000000000000000, -2.775557561562891351E-17, -1.000000000000000000 ) ) ;
#5771=EDGE_CURVE ( 'NONE', #457, #9729, #7465, .T. ) ;
#5787=SURFACE_SIDE_STYLE ('',( #702 ) ) ;
#5794=AXIS2_PLACEMENT_3D ( 'NONE', #5205, #2510, #1756 ) ;
#5803=DIRECTION ( 'NONE',  ( 0.000000000000000000, -2.775557561562888270E-17, -1.000000000000000000 ) ) ;
#5804=ORIENTED_EDGE ( 'NONE', *, *, #2410, .F. ) ;
#5817=AXIS2_PLACEMENT_3D ( 'NONE', #8228, #5753, #8282 ) ;
#5824=DIRECTION ( 'NONE',  ( 0.000000000000000000, -1.000000000000000000, 2.775557561562888270E-17 ) ) ;
#5854=EDGE_LOOP ( 'NONE', ( #2275, #6281, #5494, #10457 ) ) ;
#5865=DIRECTION ( 'NONE',  ( 1.000000000000000000, 0.000000000000000000, 0.000000000000000000 ) ) ;
#5868=CARTESIAN_POINT ( 'NONE',  ( 1.500000000000001332, 8.299669118052623479E-16, 5.525000000000000355 ) ) ;
#5875=ORIENTED_EDGE ( 'NONE', *, *, #1522, .T. ) ;
#5892=ORIENTED_EDGE ( 'NONE', *, *, #3385, .F. ) ;
#5901=ORIENTED_EDGE ( 'NONE', *, *, #10113, .T. ) ;
#5908=DIRECTION ( 'NONE',  ( 1.000000000000000000, 0.000000000000000000, 0.000000000000000000 ) ) ;
#5922=DIRECTION ( 'NONE',  ( 1.000000000000000000, 0.000000000000000000, 0.000000000000000000 ) ) ;
#5948=CARTESIAN_POINT ( 'NONE',  ( 1.500000000000001332, -1.873501354054951662E-16, -6.750000000000007994 ) ) ;
#5955=DIRECTION ( 'NONE',  ( 0.000000000000000000, -1.000000000000000000, 2.775557561562888270E-17 ) ) ;
#5957=CARTESIAN_POINT ( 'NONE',  ( -20.63749999999999574, 0.000000000000000000, 0.000000000000000000 ) ) ;
#5960=DIRECTION ( 'NONE',  ( 1.000000000000000000, 0.000000000000000000, 0.000000000000000000 ) ) ;
#5964=DIRECTION ( 'NONE',  ( 0.000000000000000000, -2.775557561562888270E-17, -1.000000000000000000 ) ) ;
#5971=DIRECTION ( 'NONE',  ( 1.000000000000000000, 0.000000000000000000, 0.000000000000000000 ) ) ;
#5977=DIRECTION ( 'NONE',  ( 1.000000000000000000, 0.000000000000000000, 0.000000000000000000 ) ) ;
#5987=DIRECTION ( 'NONE',  ( 0.000000000000000000, -2.775557561562891351E-17, -1.000000000000000000 ) ) ;
#5996=CARTESIAN_POINT ( 'NONE',  ( -0.5590169943749458970, -1.595945597898662527E-16, -5.750000000000006217 ) ) ;
#6012=VECTOR ( 'NONE', #2909, 1000.000000000000000 ) ;
#6024=CYLINDRICAL_SURFACE ( 'NONE', #5374, 6.975000000000008527 ) ;
#6033=ORIENTED_EDGE ( 'NONE', *, *, #4093, .T. ) ;
#6035=CARTESIAN_POINT ( 'NONE',  ( -1.400000000000001910, 0.000000000000000000, 0.000000000000000000 ) ) ;
#6043=CIRCLE ( 'NONE', #1278, 0.1000000000000002554 ) ;
#6052=FACE_OUTER_BOUND ( 'NONE', #6898, .T. ) ;
#6067=AXIS2_PLACEMENT_3D ( 'NONE', #7443, #8216, #4871 ) ;
#6084=FACE_OUTER_BOUND ( 'NONE', #4000, .T. ) ;
#6093=DIRECTION ( 'NONE',  ( 0.000000000000000000, -2.775557561562888270E-17, -1.000000000000000000 ) ) ;
#6121=DIRECTION ( 'NONE',  ( 1.000000000000000000, 0.000000000000000000, 0.000000000000000000 ) ) ;
#6145=CARTESIAN_POINT ( 'NONE',  ( -20.63749999999999929, -1.533495552763497570E-16, -5.525000000000006573 ) ) ;
#6149=CIRCLE ( 'NONE', #7540, 5.750000000000006217 ) ;
#6157=ORIENTED_EDGE ( 'NONE', *, *, #9566, .T. ) ;
#6174=CARTESIAN_POINT ( 'NONE',  ( 1.400000000000001910, 0.000000000000000000, 0.000000000000000000 ) ) ;
#6186=EDGE_CURVE ( 'NONE', #7276, #6230, #8314, .T. ) ;
#6188=CARTESIAN_POINT ( 'NONE',  ( 1.399999999999998579, 0.000000000000000000, 0.000000000000000000 ) ) ;
#6204=CARTESIAN_POINT ( 'NONE',  ( -20.63749999999999574, 1.126651916477732829E-15, 7.500000000000007994 ) ) ;
#6230=VERTEX_POINT ( 'NONE', #10164 ) ;
#6248=AXIS2_PLACEMENT_3D ( 'NONE', #4340, #8642, #7704 ) ;
#6267=ADVANCED_FACE ( 'NONE', ( #1177, #4607 ), #232, .T. ) ;
#6281=ORIENTED_EDGE ( 'NONE', *, *, #3587, .T. ) ;
#6292=DIRECTION ( 'NONE',  ( 0.000000000000000000, -1.000000000000000000, 2.775557561562888270E-17 ) ) ;
#6320=EDGE_CURVE ( 'NONE', #2942, #4797, #3593, .T. ) ;
#6324=DIRECTION ( 'NONE',  ( 1.000000000000000000, 0.000000000000000000, 0.000000000000000000 ) ) ;
#6347=FACE_OUTER_BOUND ( 'NONE', #4476, .T. ) ;
#6373=AXIS2_PLACEMENT_3D ( 'NONE', #8499, #10218, #108 ) ;
#6375=LINE ( 'NONE', #7972, #5488 ) ;
#6415=ADVANCED_FACE ( 'NONE', ( #823 ), #3371, .T. ) ;
#6424=CIRCLE ( 'NONE', #7841, 5.525000000000006573 ) ;
#6449=ORIENTED_EDGE ( 'NONE', *, *, #4093, .F. ) ;
#6452=CARTESIAN_POINT ( 'NONE',  ( -1.399999999999998579, 1.111629890924696344E-15, 7.400000000000007461 ) ) ;
#6460=LINE ( 'NONE', #9812, #1257 ) ;
#6477=DIRECTION ( 'NONE',  ( 0.000000000000000000, 2.775557561562888270E-17, 1.000000000000000000 ) ) ;
#6488=DIRECTION ( 'NONE',  ( 0.000000000000000000, -2.775557561562888270E-17, -1.000000000000000000 ) ) ;
#6500=CYLINDRICAL_SURFACE ( 'NONE', #749, 6.750000000000007994 ) ;
#6523=CIRCLE ( 'NONE', #7941, 0.1000000000000002554 ) ;
#6534=CARTESIAN_POINT ( 'NONE',  ( -1.399999999999998579, 0.000000000000000000, 0.000000000000000000 ) ) ;
#6540=CIRCLE ( 'NONE', #4963, 6.750000000000007994 ) ;
#6546=CARTESIAN_POINT ( 'NONE',  ( 0.000000000000000000, 0.000000000000000000, 0.000000000000000000 ) ) ;
#6566=VERTEX_POINT ( 'NONE', #8046 ) ;
#6588=EDGE_CURVE ( 'NONE', #7276, #9464, #6043, .T. ) ;
#6610=ADVANCED_FACE ( 'NONE', ( #6347 ), #6500, .F. ) ;
#6613=LINE ( 'NONE', #1518, #4304 ) ;
#6630=ORIENTED_EDGE ( 'NONE', *, *, #2219, .F. ) ;
#6632=FACE_OUTER_BOUND ( 'NONE', #2273, .T. ) ;
#6636=DIRECTION ( 'NONE',  ( -1.000000000000000000, 0.000000000000000000, 0.000000000000000000 ) ) ;
#6654=EDGE_CURVE ( 'NONE', #856, #457, #1631, .T. ) ;
#6669=DIRECTION ( 'NONE',  ( 0.000000000000000000, 1.502202555303639631E-16, 1.000000000000000000 ) ) ;
#6674=EDGE_LOOP ( 'NONE', ( #1417, #6831, #2445, #9262 ) ) ;
#6685=ORIENTED_EDGE ( 'NONE', *, *, #4714, .T. ) ;
#6686=CIRCLE ( 'NONE', #860, 0.1000000000000002554 ) ;
#6705=ORIENTED_EDGE ( 'NONE', *, *, #7210, .T. ) ;
#6722=EDGE_CURVE ( 'NONE', #4407, #631, #1453, .T. ) ;
#6780=ORIENTED_EDGE ( 'NONE', *, *, #6320, .T. ) ;
#6805=DIRECTION ( 'NONE',  ( 0.000000000000000000, -2.775557561562888270E-17, -1.000000000000000000 ) ) ;
#6812=CARTESIAN_POINT ( 'NONE',  ( -1.399999999999998579, 0.000000000000000000, 0.000000000000000000 ) ) ;
#6817=UNCERTAINTY_MEASURE_WITH_UNIT (LENGTH_MEASURE( 1.000000000000000082E-05 ), #4912, 'distance_accuracy_value', 'NONE');
#6831=ORIENTED_EDGE ( 'NONE', *, *, #8022, .T. ) ;
#6835=ORIENTED_EDGE ( 'NONE', *, *, #3700, .T. ) ;
#6845=VERTEX_POINT ( 'NONE', #813 ) ;
#6853=TOROIDAL_SURFACE ( 'NONE', #9506, 6.250000000000000000, 0.7500000000000000000 ) ;
#6863=CYLINDRICAL_SURFACE ( 'NONE', #10106, 7.500000000000007994 ) ;
#6870=EDGE_CURVE ( 'NONE', #1394, #9698, #3192, .T. ) ;
#6874=ADVANCED_FACE ( 'NONE', ( #87 ), #9203, .T. ) ;
#6890=ORIENTED_EDGE ( 'NONE', *, *, #1657, .T. ) ;
#6898=EDGE_LOOP ( 'NONE', ( #4183, #3318, #8686, #271 ) ) ;
#6906=CIRCLE ( 'NONE', #6373, 5.000000000000005329 ) ;
#6945=AXIS2_PLACEMENT_3D ( 'NONE', #9745, #2389, #4006 ) ;
#6959=DIRECTION ( 'NONE',  ( 0.000000000000000000, -2.775557561562887961E-17, -1.000000000000000000 ) ) ;
#6980=DIRECTION ( 'NONE',  ( 0.000000000000000000, -2.775557561562888270E-17, -1.000000000000000000 ) ) ;
#6982=ORIENTED_EDGE ( 'NONE', *, *, #4994, .T. ) ;
#6998=CARTESIAN_POINT ( 'NONE',  ( 0.5590169943749494497, 6.392864540189691546E-16, -6.750000000000007105 ) ) ;
#7014=EDGE_CURVE ( 'NONE', #3713, #9729, #409, .T. ) ;
#7040=AXIS2_PLACEMENT_3D ( 'NONE', #1904, #3431, #7048 ) ;
#7048=DIRECTION ( 'NONE',  ( 1.000000000000000000, 0.000000000000000000, 0.000000000000000000 ) ) ;
#7083=AXIS2_PLACEMENT_3D ( 'NONE', #2178, #5558, #2790 ) ;
#7106=EDGE_CURVE ( 'NONE', #8744, #6845, #948, .T. ) ;
#7112=AXIS2_PLACEMENT_3D ( 'NONE', #1699, #9254, #4142 ) ;
#7135=ADVANCED_FACE ( 'NONE', ( #1603 ), #6863, .T. ) ;
#7141=LINE ( 'NONE', #10500, #6012 ) ;
#7142=ADVANCED_FACE ( 'NONE', ( #8392 ), #3771, .T. ) ;
#7143=DIRECTION ( 'NONE',  ( 0.000000000000000000, -2.775557561562887961E-17, -1.000000000000000000 ) ) ;
#7146=VERTEX_POINT ( 'NONE', #5156 ) ;
#7159=ORIENTED_EDGE ( 'NONE', *, *, #4669, .T. ) ;
#7207=DIRECTION ( 'NONE',  ( 1.000000000000000000, 0.000000000000000000, 0.000000000000000000 ) ) ;
#7210=EDGE_CURVE ( 'NONE', #856, #3713, #1823, .T. ) ;
#7268=DIRECTION ( 'NONE',  ( 0.000000000000000000, 2.775557561562888270E-17, 1.000000000000000000 ) ) ;
#7276=VERTEX_POINT ( 'NONE', #2008 ) ;
#7277=AXIS2_PLACEMENT_3D ( 'NONE', #756, #4803, #2400 ) ;
#7330=VERTEX_POINT ( 'NONE', #9931 ) ;
#7351=STYLED_ITEM ( 'NONE', ( #7863 ), #4934 ) ;
#7352=ORIENTED_EDGE ( 'NONE', *, *, #6186, .T. ) ;
#7365=ORIENTED_EDGE ( 'NONE', *, *, #4714, .F. ) ;
#7374=DIRECTION ( 'NONE',  ( 1.000000000000000000, 0.000000000000000000, 0.000000000000000000 ) ) ;
#7405=AXIS2_PLACEMENT_3D ( 'NONE', #7671, #5960, #1648 ) ;
#7419=DIRECTION ( 'NONE',  ( 0.000000000000000000, 1.000000000000000000, 9.470910429910644418E-17 ) ) ;
#7443=CARTESIAN_POINT ( 'NONE',  ( -1.500000000000001332, 0.000000000000000000, 0.000000000000000000 ) ) ;
#7445=AXIS2_PLACEMENT_3D ( 'NONE', #3662, #4273, #9342 ) ;
#7458=DIRECTION ( 'NONE',  ( 1.000000000000000000, 0.000000000000000000, 0.000000000000000000 ) ) ;
#7465=CIRCLE ( 'NONE', #7277, 5.000000000000005329 ) ;
#7471=ORIENTED_EDGE ( 'NONE', *, *, #10331, .T. ) ;
#7507=ORIENTED_EDGE ( 'NONE', *, *, #5395, .T. ) ;
#7533=ADVANCED_FACE ( 'NONE', ( #10210 ), #6024, .F. ) ;
#7539=EDGE_CURVE ( 'NONE', #1765, #457, #7609, .T. ) ;
#7540=AXIS2_PLACEMENT_3D ( 'NONE', #10253, #6121, #7886 ) ;
#7549=EDGE_LOOP ( 'NONE', ( #1111, #6890, #8385, #2894 ) ) ;
#7609=LINE ( 'NONE', #8551, #9755 ) ;
#7612=SHAPE_REPRESENTATION ( 'angular contact ball bearing_68_iso_ISO 15 ABB - 1710 - 20,SI,NC,20_68', ( #7040 ), #4727 ) ;
#7618=CARTESIAN_POINT ( 'NONE',  ( -1.400000000000001910, 0.000000000000000000, 0.000000000000000000 ) ) ;
#7631=ORIENTED_EDGE ( 'NONE', *, *, #4313, .T. ) ;
#7637=CARTESIAN_POINT ( 'NONE',  ( 0.1920286436967143240, 1.533495552763497570E-16, 5.525000000000006573 ) ) ;
#7644=DIRECTION ( 'NONE',  ( 0.000000000000000000, 2.775557561562888270E-17, 1.000000000000000000 ) ) ;
#7654=DIRECTION ( 'NONE',  ( 0.000000000000000000, -2.775557561562888270E-17, -1.000000000000000000 ) ) ;
#7662=ORIENTED_EDGE ( 'NONE', *, *, #9566, .F. ) ;
#7671=CARTESIAN_POINT ( 'NONE',  ( -1.500000000000001332, 0.000000000000000000, 0.000000000000000000 ) ) ;
#7679=FACE_OUTER_BOUND ( 'NONE', #10063, .T. ) ;
#7704=DIRECTION ( 'NONE',  ( 0.000000000000000000, -2.775557561562888270E-17, -1.000000000000000000 ) ) ;
#7722=CLOSED_SHELL ( 'NONE', ( #3550, #2993, #10081, #7533, #8640, #602, #7142, #774, #105, #10275, #2888, #3542, #6415, #5574, #4921, #3139, #5724, #1377, #6874, #6267, #8600, #6610, #10562, #5126, #7135, #2880, #9291, #3756 ) ) ;
#7775=CARTESIAN_POINT ( 'NONE',  ( -20.63749999999999929, 0.000000000000000000, 0.000000000000000000 ) ) ;
#7782=AXIS2_PLACEMENT_3D ( 'NONE', #2372, #8223, #9780 ) ;
#7789=CARTESIAN_POINT ( 'NONE',  ( -1.500000000000001332, 1.047786282324290395E-15, 6.975000000000000533 ) ) ;
#7808=AXIS2_PLACEMENT_3D ( 'NONE', #5216, #7458, #5803 ) ;
#7809=ORIENTED_EDGE ( 'NONE', *, *, #5771, .F. ) ;
#7826=CIRCLE ( 'NONE', #9922, 0.7499999999999997780 ) ;
#7841=AXIS2_PLACEMENT_3D ( 'NONE', #8653, #9600, #2034 ) ;
#7863=PRESENTATION_STYLE_ASSIGNMENT (( #4378 ) ) ;
#7874=DIRECTION ( 'NONE',  ( 0.000000000000000000, -2.775557561562887961E-17, -1.000000000000000000 ) ) ;
#7878=DIRECTION ( 'NONE',  ( -1.000000000000000000, 0.000000000000000000, 0.000000000000000000 ) ) ;
#7882=ORIENTED_EDGE ( 'NONE', *, *, #8939, .F. ) ;
#7886=DIRECTION ( 'NONE',  ( 0.000000000000000000, -2.775557561562888270E-17, -1.000000000000000000 ) ) ;
#7893=DIRECTION ( 'NONE',  ( 1.000000000000000000, 0.000000000000000000, 0.000000000000000000 ) ) ;
#7894=DIRECTION ( 'NONE',  ( 0.000000000000000000, -2.775557561562887961E-17, -1.000000000000000000 ) ) ;
#7941=AXIS2_PLACEMENT_3D ( 'NONE', #3240, #9947, #5708 ) ;
#7944=PRODUCT_DEFINITION_SHAPE ( 'NONE', 'NONE',  #4432 ) ;
#7956=VERTEX_POINT ( 'NONE', #5948 ) ;
#7957=CIRCLE ( 'NONE', #9714, 5.100000000000006750 ) ;
#7962=CARTESIAN_POINT ( 'NONE',  ( -1.500000000000001332, 5.750000000000006217, -2.168404344971008868E-16 ) ) ;
#7972=CARTESIAN_POINT ( 'NONE',  ( -20.63749999999999929, 8.299669118052633340E-16, 5.525000000000006573 ) ) ;
#7987=DIRECTION ( 'NONE',  ( -1.000000000000000000, -0.000000000000000000, -0.000000000000000000 ) ) ;
#7994=AXIS2_PLACEMENT_3D ( 'NONE', #2476, #5865, #7143 ) ;
#8022=EDGE_CURVE ( 'NONE', #3515, #1394, #1998, .T. ) ;
#8028=CYLINDRICAL_SURFACE ( 'NONE', #9130, 5.000000000000005329 ) ;
#8038=UNCERTAINTY_MEASURE_WITH_UNIT (LENGTH_MEASURE( 1.000000000000000082E-05 ), #3651, 'distance_accuracy_value', 'NONE');
#8045=ORIENTED_EDGE ( 'NONE', *, *, #1203, .T. ) ;
#8046=CARTESIAN_POINT ( 'NONE',  ( -1.500000000000001776, -1.415534356397074737E-16, -5.100000000000006750 ) ) ;
#8056=LINE ( 'NONE', #9770, #3714 ) ;
#8097=DIRECTION ( 'NONE',  ( 0.000000000000000000, -2.775557561562887961E-17, -1.000000000000000000 ) ) ;
#8114=ORIENTED_EDGE ( 'NONE', *, *, #4903, .F. ) ;
#8122=CARTESIAN_POINT ( 'NONE',  ( 0.1920286436967143240, 5.812771276357657970E-16, -5.525000000000000355 ) ) ;
#8134=ORIENTED_EDGE ( 'NONE', *, *, #6722, .T. ) ;
#8138=UNCERTAINTY_MEASURE_WITH_UNIT (LENGTH_MEASURE( 1.000000000000000082E-05 ), #2638, 'distance_accuracy_value', 'NONE');
#8142=DIRECTION ( 'NONE',  ( 1.000000000000000000, 0.000000000000000000, 0.000000000000000000 ) ) ;
#8154=AXIS2_PLACEMENT_3D ( 'NONE', #3268, #4961, #6669 ) ;
#8199=ORIENTED_EDGE ( 'NONE', *, *, #10120, .F. ) ;
#8216=DIRECTION ( 'NONE',  ( 1.000000000000000000, 0.000000000000000000, 0.000000000000000000 ) ) ;
#8223=DIRECTION ( 'NONE',  ( 1.000000000000000000, 0.000000000000000000, 0.000000000000000000 ) ) ;
#8228=CARTESIAN_POINT ( 'NONE',  ( 1.399999999999998579, 0.000000000000000000, 0.000000000000000000 ) ) ;
#8262=EDGE_CURVE ( 'NONE', #9698, #1394, #5179, .T. ) ;
#8282=DIRECTION ( 'NONE',  ( 0.000000000000000000, -2.775557561562888270E-17, -1.000000000000000000 ) ) ;
#8314=CIRCLE ( 'NONE', #7808, 7.400000000000007461 ) ;
#8334=ORIENTED_EDGE ( 'NONE', *, *, #7539, .T. ) ;
#8365=ORIENTED_EDGE ( 'NONE', *, *, #2129, .F. ) ;
#8385=ORIENTED_EDGE ( 'NONE', *, *, #6654, .T. ) ;
#8392=FACE_OUTER_BOUND ( 'NONE', #10453, .T. ) ;
#8394=CARTESIAN_POINT ( 'NONE',  ( -0.5590169943749458970, 0.000000000000000000, 0.000000000000000000 ) ) ;
#8395=DIRECTION ( 'NONE',  ( 0.000000000000000000, -2.775557561562888270E-17, -1.000000000000000000 ) ) ;
#8397=ORIENTED_EDGE ( 'NONE', *, *, #9822, .T. ) ;
#8412=CARTESIAN_POINT ( 'NONE',  ( -1.400000000000001910, 7.661233032048583711E-16, 5.100000000000006750 ) ) ;
#8417=EDGE_LOOP ( 'NONE', ( #5587, #550, #9796, #10203 ) ) ;
#8419=AXIS2_PLACEMENT_3D ( 'NONE', #6174, #3562, #5187 ) ;
#8456=DIRECTION ( 'NONE',  ( 1.000000000000000000, 0.000000000000000000, 0.000000000000000000 ) ) ;
#8461=AXIS2_PLACEMENT_3D ( 'NONE', #610, #4928, #2212 ) ;
#8471=AXIS2_PLACEMENT_3D ( 'NONE', #1234, #1290, #9577 ) ;
#8488=TOROIDAL_SURFACE ( 'NONE', #8845, 6.250000000000000000, 0.7500000000000000000 ) ;
#8493=DIRECTION ( 'NONE',  ( 1.000000000000000000, 0.000000000000000000, 0.000000000000000000 ) ) ;
#8494=DIRECTION ( 'NONE',  ( 1.000000000000000000, 0.000000000000000000, 0.000000000000000000 ) ) ;
#8499=CARTESIAN_POINT ( 'NONE',  ( -1.400000000000001910, 0.000000000000000000, 0.000000000000000000 ) ) ;
#8520=AXIS2_PLACEMENT_3D ( 'NONE', #10578, #2990, #519 ) ;
#8551=CARTESIAN_POINT ( 'NONE',  ( -20.63749999999999929, -1.387778780781445676E-16, -5.000000000000005329 ) ) ;
#8557=FACE_OUTER_BOUND ( 'NONE', #3763, .T. ) ;
#8562=FILL_AREA_STYLE_COLOUR ( '', #4564 ) ;
#8580=CYLINDRICAL_SURFACE ( 'NONE', #10261, 6.750000000000007994 ) ;
#8585=VERTEX_POINT ( 'NONE', #10133 ) ;
#8590=CARTESIAN_POINT ( 'NONE',  ( 1.500000000000001332, 0.000000000000000000, 0.000000000000000000 ) ) ;
#8600=ADVANCED_FACE ( 'NONE', ( #10858 ), #8488, .T. ) ;
#8620=VERTEX_POINT ( 'NONE', #6998 ) ;
#8628=FACE_OUTER_BOUND ( 'NONE', #2051, .T. ) ;
#8640=ADVANCED_FACE ( 'NONE', ( #9415 ), #8580, .F. ) ;
#8642=DIRECTION ( 'NONE',  ( 1.000000000000000000, 0.000000000000000000, 0.000000000000000000 ) ) ;
#8653=CARTESIAN_POINT ( 'NONE',  ( 0.1920286436967143240, 0.000000000000000000, 0.000000000000000000 ) ) ;
#8676=DIRECTION ( 'NONE',  ( 1.000000000000000000, 0.000000000000000000, 0.000000000000000000 ) ) ;
#8686=ORIENTED_EDGE ( 'NONE', *, *, #7106, .T. ) ;
#8728=ORIENTED_EDGE ( 'NONE', *, *, #10865, .T. ) ;
#8736=DIRECTION ( 'NONE',  ( 1.000000000000000000, 0.000000000000000000, 0.000000000000000000 ) ) ;
#8744=VERTEX_POINT ( 'NONE', #5996 ) ;
#8765=CARTESIAN_POINT ( 'NONE',  ( 1.500000000000001332, 0.000000000000000000, 0.000000000000000000 ) ) ;
#8785=ORIENTED_EDGE ( 'NONE', *, *, #4313, .F. ) ;
#8807=EDGE_LOOP ( 'NONE', ( #3889, #8134 ) ) ;
#8811=CARTESIAN_POINT ( 'NONE',  ( -20.63749999999999929, -1.595945597898662527E-16, -5.750000000000006217 ) ) ;
#8845=AXIS2_PLACEMENT_3D ( 'NONE', #6546, #3311, #7644 ) ;
#8864=AXIS2_PLACEMENT_3D ( 'NONE', #8590, #3506, #7654 ) ;
#8866=DIRECTION ( 'NONE',  ( 0.000000000000000000, -9.470910429910653047E-17, 1.000000000000000000 ) ) ;
#8878=AXIS2_PLACEMENT_3D ( 'NONE', #7775, #5299, #10365 ) ;
#8894=DIRECTION ( 'NONE',  ( 1.000000000000000000, 0.000000000000000000, 0.000000000000000000 ) ) ;
#8901=ORIENTED_EDGE ( 'NONE', *, *, #4051, .F. ) ;
#8907=DIRECTION ( 'NONE',  ( 1.000000000000000000, 0.000000000000000000, 0.000000000000000000 ) ) ;
#8912=ORIENTED_EDGE ( 'NONE', *, *, #9892, .F. ) ;
#8921=EDGE_LOOP ( 'NONE', ( #5629, #3917 ) ) ;
#8929=CARTESIAN_POINT ( 'NONE',  ( -1.399999999999998579, -2.081668171172168513E-16, -7.500000000000007994 ) ) ;
#8930=APPLICATION_CONTEXT ( 'automotive_design' ) ;
#8939=EDGE_CURVE ( 'NONE', #6845, #8744, #10618, .T. ) ;
#8981=DIRECTION ( 'NONE',  ( 1.000000000000000000, 0.000000000000000000, 0.000000000000000000 ) ) ;
#8982=DIRECTION ( 'NONE',  ( 1.000000000000000000, 0.000000000000000000, 0.000000000000000000 ) ) ;
#9005=FACE_OUTER_BOUND ( 'NONE', #5628, .T. ) ;
#9015=DIRECTION ( 'NONE',  ( 0.000000000000000000, -2.775557561562888270E-17, -1.000000000000000000 ) ) ;
#9017=ORIENTED_EDGE ( 'NONE', *, *, #3282, .T. ) ;
#9038=VERTEX_POINT ( 'NONE', #5868 ) ;
#9052=( NAMED_UNIT ( * ) SI_UNIT ( $, .STERADIAN. ) SOLID_ANGLE_UNIT ( ) );
#9067=LINE ( 'NONE', #666, #9862 ) ;
#9070=DIRECTION ( 'NONE',  ( 1.000000000000000000, 0.000000000000000000, 0.000000000000000000 ) ) ;
#9130=AXIS2_PLACEMENT_3D ( 'NONE', #1191, #8907, #10465 ) ;
#9154=ORIENTED_EDGE ( 'NONE', *, *, #3124, .T. ) ;
#9186=DIRECTION ( 'NONE',  ( 0.000000000000000000, 1.000000000000000000, -1.502202555303642096E-16 ) ) ;
#9192=DIRECTION ( 'NONE',  ( 0.000000000000000000, -2.775557561562887961E-17, -1.000000000000000000 ) ) ;
#9203=TOROIDAL_SURFACE ( 'NONE', #4108, 5.100000000000000533, 0.1000000000000001582 ) ;
#9217=LINE ( 'NONE', #4372, #10759 ) ;
#9224=CIRCLE ( 'NONE', #1141, 6.975000000000008527 ) ;
#9226=DIRECTION ( 'NONE',  ( 1.000000000000000000, 0.000000000000000000, 0.000000000000000000 ) ) ;
#9254=DIRECTION ( 'NONE',  ( -1.000000000000000000, 0.000000000000000000, 0.000000000000000000 ) ) ;
#9262=ORIENTED_EDGE ( 'NONE', *, *, #2406, .F. ) ;
#9271=DIRECTION ( 'NONE',  ( 0.000000000000000000, -2.775557561562888270E-17, -1.000000000000000000 ) ) ;
#9291=ADVANCED_FACE ( 'NONE', ( #3107, #4022 ), #4804, .T. ) ;
#9300=CIRCLE ( 'NONE', #2587, 5.000000000000005329 ) ;
#9320=VERTEX_POINT ( 'NONE', #8929 ) ;
#9339=ORIENTED_EDGE ( 'NONE', *, *, #3618, .T. ) ;
#9342=DIRECTION ( 'NONE',  ( 0.000000000000000000, 2.775557561562887961E-17, 1.000000000000000000 ) ) ;
#9348=AXIS2_PLACEMENT_3D ( 'NONE', #5528, #8894, #9621 ) ;
#9349=CIRCLE ( 'NONE', #5132, 5.000000000000005329 ) ;
#9350=ORIENTED_EDGE ( 'NONE', *, *, #6588, .F. ) ;
#9368=AXIS2_PLACEMENT_3D ( 'NONE', #517, #7207, #10576 ) ;
#9392=EDGE_LOOP ( 'NONE', ( #3922, #6685, #6157, #5901 ) ) ;
#9407=CARTESIAN_POINT ( 'NONE',  ( -1.500000000000001332, 0.000000000000000000, 0.000000000000000000 ) ) ;
#9415=FACE_OUTER_BOUND ( 'NONE', #8417, .T. ) ;
#9428=CARTESIAN_POINT ( 'NONE',  ( -1.400000000000001910, 0.000000000000000000, 0.000000000000000000 ) ) ;
#9448=CARTESIAN_POINT ( 'NONE',  ( -20.63749999999999929, 0.000000000000000000, 0.000000000000000000 ) ) ;
#9453=PLANE ( 'NONE',  #2120 ) ;
#9458=( NAMED_UNIT ( * ) PLANE_ANGLE_UNIT ( ) SI_UNIT ( $, .RADIAN. ) );
#9464=VERTEX_POINT ( 'NONE', #27 ) ;
#9489=CARTESIAN_POINT ( 'NONE',  ( 0.000000000000000000, 1.734723475976807094E-16, 6.250000000000007105 ) ) ;
#9492=AXIS2_PLACEMENT_3D ( 'NONE', #5957, #4244, #5080 ) ;
#9506=AXIS2_PLACEMENT_3D ( 'NONE', #4523, #7878, #1085 ) ;
#9531=DIRECTION ( 'NONE',  ( 1.000000000000000000, 0.000000000000000000, 0.000000000000000000 ) ) ;
#9533=CIRCLE ( 'NONE', #4765, 6.750000000000007994 ) ;
#9566=EDGE_CURVE ( 'NONE', #10165, #4640, #4817, .T. ) ;
#9577=DIRECTION ( 'NONE',  ( 0.000000000000000000, -2.775557561562888270E-17, -1.000000000000000000 ) ) ;
#9600=DIRECTION ( 'NONE',  ( -1.000000000000000000, 0.000000000000000000, 0.000000000000000000 ) ) ;
#9605=ORIENTED_EDGE ( 'NONE', *, *, #4030, .T. ) ;
#9615=ORIENTED_EDGE ( 'NONE', *, *, #7014, .T. ) ;
#9621=DIRECTION ( 'NONE',  ( 0.000000000000000000, -2.775557561562888270E-17, -1.000000000000000000 ) ) ;
#9641=ORIENTED_EDGE ( 'NONE', *, *, #3176, .T. ) ;
#9693=DIRECTION ( 'NONE',  ( 0.000000000000000000, -2.775557561562888270E-17, -1.000000000000000000 ) ) ;
#9698=VERTEX_POINT ( 'NONE', #578 ) ;
#9700=CIRCLE ( 'NONE', #9368, 7.500000000000007994 ) ;
#9714=AXIS2_PLACEMENT_3D ( 'NONE', #3685, #7893, #1868 ) ;
#9729=VERTEX_POINT ( 'NONE', #3099 ) ;
#9745=CARTESIAN_POINT ( 'NONE',  ( -1.500000000000001332, 0.000000000000000000, 0.000000000000000000 ) ) ;
#9749=LINE ( 'NONE', #8811, #10768 ) ;
#9755=VECTOR ( 'NONE', #5908, 1000.000000000000000 ) ;
#9770=CARTESIAN_POINT ( 'NONE',  ( -20.63749999999999574, -1.935951399190116865E-16, -6.975000000000008527 ) ) ;
#9780=DIRECTION ( 'NONE',  ( 0.000000000000000000, -2.775557561562888270E-17, -1.000000000000000000 ) ) ;
#9788=EDGE_LOOP ( 'NONE', ( #8785, #10045 ) ) ;
#9796=ORIENTED_EDGE ( 'NONE', *, *, #2219, .T. ) ;
#9803=DIRECTION ( 'NONE',  ( 0.000000000000000000, 1.502202555303639631E-16, 1.000000000000000000 ) ) ;
#9812=CARTESIAN_POINT ( 'NONE',  ( -20.63749999999999574, -2.081668171172168513E-16, -7.500000000000007994 ) ) ;
#9822=EDGE_CURVE ( 'NONE', #1765, #6566, #5000, .T. ) ;
#9826=( GEOMETRIC_REPRESENTATION_CONTEXT ( 3 ) GLOBAL_UNCERTAINTY_ASSIGNED_CONTEXT ( ( #6817 ) ) GLOBAL_UNIT_ASSIGNED_CONTEXT ( ( #4912, #2404, #9052 ) ) REPRESENTATION_CONTEXT ( 'NONE', 'WORKASPACE' ) );
#9848=DIRECTION ( 'NONE',  ( 1.000000000000000000, 0.000000000000000000, 0.000000000000000000 ) ) ;
#9862=VECTOR ( 'NONE', #4046, 1000.000000000000000 ) ;
#9879=EDGE_CURVE ( 'NONE', #4112, #8744, #7826, .T. ) ;
#9881=FACE_OUTER_BOUND ( 'NONE', #5854, .T. ) ;
#9892=EDGE_CURVE ( 'NONE', #5286, #2789, #415, .T. ) ;
#9893=ORIENTED_EDGE ( 'NONE', *, *, #1814, .F. ) ;
#9916=CARTESIAN_POINT ( 'NONE',  ( 0.1920286436967143240, 0.000000000000000000, 0.000000000000000000 ) ) ;
#9922=AXIS2_PLACEMENT_3D ( 'NONE', #744, #2442, #3437 ) ;
#9931=CARTESIAN_POINT ( 'NONE',  ( -0.1920286436967143240, 1.935951399190116865E-16, 6.975000000000007638 ) ) ;
#9947=DIRECTION ( 'NONE',  ( 0.000000000000000000, -1.000000000000000000, 2.775557561562888270E-17 ) ) ;
#9987=ORIENTED_EDGE ( 'NONE', *, *, #1455, .F. ) ;
#10036=FILL_AREA_STYLE_COLOUR ( '', #10715 ) ;
#10045=ORIENTED_EDGE ( 'NONE', *, *, #94, .F. ) ;
#10063=EDGE_LOOP ( 'NONE', ( #7631, #6835, #3697, #9893 ) ) ;
#10081=ADVANCED_FACE ( 'NONE', ( #5293 ), #5365, .T. ) ;
#10106=AXIS2_PLACEMENT_3D ( 'NONE', #1838, #1777, #1713 ) ;
#10113=EDGE_CURVE ( 'NONE', #4640, #8620, #2009, .T. ) ;
#10120=EDGE_CURVE ( 'NONE', #6566, #2789, #10818, .T. ) ;
#10122=ORIENTED_EDGE ( 'NONE', *, *, #3066, .F. ) ;
#10133=CARTESIAN_POINT ( 'NONE',  ( 1.500000000000001332, 1.013986724829958402E-15, 6.750000000000000000 ) ) ;
#10162=CARTESIAN_POINT ( 'NONE',  ( 1.500000000000001332, 5.100000000000004974, 0.000000000000000000 ) ) ;
#10164=CARTESIAN_POINT ( 'NONE',  ( -1.500000000000001332, -2.053912595556539452E-16, -7.400000000000007461 ) ) ;
#10165=VERTEX_POINT ( 'NONE', #7637 ) ;
#10168=DIRECTION ( 'NONE',  ( 0.000000000000000000, -2.775557561562887961E-17, -1.000000000000000000 ) ) ;
#10192=STYLED_ITEM ( 'NONE', ( #1527 ), #10510 ) ;
#10203=ORIENTED_EDGE ( 'NONE', *, *, #2722, .F. ) ;
#10210=FACE_OUTER_BOUND ( 'NONE', #1392, .T. ) ;
#10218=DIRECTION ( 'NONE',  ( 1.000000000000000000, 0.000000000000000000, 0.000000000000000000 ) ) ;
#10241=CARTESIAN_POINT ( 'NONE',  ( -1.500000000000001332, -1.935951399190116865E-16, -6.975000000000008527 ) ) ;
#10253=CARTESIAN_POINT ( 'NONE',  ( -1.500000000000001332, 0.000000000000000000, 0.000000000000000000 ) ) ;
#10255=DIRECTION ( 'NONE',  ( 1.000000000000000000, 0.000000000000000000, 0.000000000000000000 ) ) ;
#10261=AXIS2_PLACEMENT_3D ( 'NONE', #5236, #9531, #2716 ) ;
#10275=ADVANCED_FACE ( 'NONE', ( #7679 ), #4319, .T. ) ;
#10331=EDGE_CURVE ( 'NONE', #9729, #457, #9300, .T. ) ;
#10344=CARTESIAN_POINT ( 'NONE',  ( -1.400000000000001910, 7.511012776518211958E-16, 5.000000000000000000 ) ) ;
#10347=CARTESIAN_POINT ( 'NONE',  ( 1.500000000000001332, 1.119140903701213403E-15, 7.399999999999999467 ) ) ;
#10365=DIRECTION ( 'NONE',  ( 0.000000000000000000, -2.775557561562888270E-17, -1.000000000000000000 ) ) ;
#10384=CIRCLE ( 'NONE', #1218, 0.7499999999999997780 ) ;
#10420=FACE_OUTER_BOUND ( 'NONE', #1577, .T. ) ;
#10426=CIRCLE ( 'NONE', #8471, 6.975000000000008527 ) ;
#10431=AXIS2_PLACEMENT_3D ( 'NONE', #6534, #413, #9015 ) ;
#10437=FACE_OUTER_BOUND ( 'NONE', #7549, .T. ) ;
#10453=EDGE_LOOP ( 'NONE', ( #9154, #3353, #8199, #2396 ) ) ;
#10457=ORIENTED_EDGE ( 'NONE', *, *, #6870, .F. ) ;
#10465=DIRECTION ( 'NONE',  ( 0.000000000000000000, -2.775557561562888270E-17, -1.000000000000000000 ) ) ;
#10466=AXIS2_PLACEMENT_3D ( 'NONE', #431, #4799, #638 ) ;
#10477=TOROIDAL_SURFACE ( 'NONE', #3391, 5.100000000000000533, 0.1000000000000001582 ) ;
#10494=ORIENTED_EDGE ( 'NONE', *, *, #4669, .F. ) ;
#10496=CARTESIAN_POINT ( 'NONE',  ( 0.5590169943749494497, 0.000000000000000000, 0.000000000000000000 ) ) ;
#10499=ORIENTED_EDGE ( 'NONE', *, *, #4030, .F. ) ;
#10500=CARTESIAN_POINT ( 'NONE',  ( -20.63749999999999929, 7.511012776518219847E-16, 5.000000000000005329 ) ) ;
#10510=MANIFOLD_SOLID_BREP ( 'OuterRace', #7722 ) ;
#10562=ADVANCED_FACE ( 'NONE', ( #6084 ), #1482, .F. ) ;
#10576=DIRECTION ( 'NONE',  ( 0.000000000000000000, -2.775557561562888270E-17, -1.000000000000000000 ) ) ;
#10578=CARTESIAN_POINT ( 'NONE',  ( 1.400000000000001910, 7.661233032048583711E-16, 5.100000000000006750 ) ) ;
#10587=PRODUCT ( 'angular contact ball bearing_68_iso_ISO 15 ABB - 1710 - 20,SI,NC,20_68', 'angular contact ball bearing_68_iso_ISO 15 ABB - 1710 - 20,SI,NC,20_68', '', ( #707 ) ) ;
#10618=CIRCLE ( 'NONE', #1616, 5.750000000000006217 ) ;
#10671=CYLINDRICAL_SURFACE ( 'NONE', #4957, 7.500000000000007994 ) ;
#10715=COLOUR_RGB ( '', 0.72549020, 0.75294118, 0.79215686) ;
#10717=CYLINDRICAL_SURFACE ( 'NONE', #8461, 5.525000000000006573 ) ;
#10759=VECTOR ( 'NONE', #4257, 1000.000000000000000 ) ;
#10765=EDGE_LOOP ( 'NONE', ( #1164, #3438, #9017, #7662 ) ) ;
#10768=VECTOR ( 'NONE', #4587, 1000.000000000000000 ) ;
#10818=CIRCLE ( 'NONE', #4488, 5.100000000000006750 ) ;
#10853=DIRECTION ( 'NONE',  ( 0.000000000000000000, -1.000000000000000000, 2.775557561562888270E-17 ) ) ;
#10858=FACE_OUTER_BOUND ( 'NONE', #5554, .T. ) ;
#10863=ORIENTED_EDGE ( 'NONE', *, *, #4969, .F. ) ;
#10865=EDGE_CURVE ( 'NONE', #7330, #6845, #10384, .T. ) ;
#10869=DIRECTION ( 'NONE',  ( 1.000000000000000000, 0.000000000000000000, 0.000000000000000000 ) ) ;
#10915=ORIENTED_EDGE ( 'NONE', *, *, #3282, .F. ) ;
#10922=CARTESIAN_POINT ( 'NONE',  ( -1.500000000000001332, 0.000000000000000000, 0.000000000000000000 ) ) ;
#10937=DIRECTION ( 'NONE',  ( 0.000000000000000000, -2.775557561562888270E-17, -1.000000000000000000 ) ) ;
#10940=CYLINDRICAL_SURFACE ( 'NONE', #4117, 5.525000000000006573 ) ;
ENDSEC;
END-ISO-10303-21;
